ISO-10303-21;
HEADER;
FILE_DESCRIPTION (('STEP AP214'),
    '1' );
FILE_NAME ('Holder.step',
    '2026-10-09T10:51:02',
    ( '' ),
    ( '' ),
    'SwSTEP 2.0',
    'SolidWorks 2026',
    '' );
FILE_SCHEMA (( 'AUTOMOTIVE_DESIGN' ));
ENDSEC;

DATA;
#1=ORIENTED_EDGE ( 'NONE', *, *, #17423, .F. ) ;
#13=VECTOR ( 'NONE', #9330, 999.9999999999998863 ) ;
#38=ORIENTED_EDGE ( 'NONE', *, *, #21148, .T. ) ;
#61=AXIS2_PLACEMENT_3D ( 'NONE', #18338, #21644, #15030 ) ;
#81=ORIENTED_EDGE ( 'NONE', *, *, #8487, .T. ) ;
#205=PLANE ( 'NONE',  #10305 ) ;
#297=VECTOR ( 'NONE', #9208, 1000.000000000000114 ) ;
#310=CARTESIAN_POINT ( 'NONE',  ( -55.33894950108835076, 126.9191314136037789, 167.5679852142818334 ) ) ;
#353=CARTESIAN_POINT ( 'NONE',  ( -42.64894290516974706, 118.1474297122749135, 27.43850586800562752 ) ) ;
#434=EDGE_LOOP ( 'NONE', ( #5198, #13858 ) ) ;
#492=LINE ( 'NONE', #7494, #7808 ) ;
#625=DIRECTION ( 'NONE',  ( 0.01292394549866637994, 0.005513023399719273882, 0.9999012842304692006 ) ) ;
#630=DIRECTION ( 'NONE',  ( -0.01292394549866624984, -0.005513023399719273882, -0.9999012842304693116 ) ) ;
#737=CIRCLE ( 'NONE', #6941, 3.099999999999998757 ) ;
#834=ORIENTED_EDGE ( 'NONE', *, *, #11044, .F. ) ;
#858=VERTEX_POINT ( 'NONE', #2285 ) ;
#882=AXIS2_PLACEMENT_3D ( 'NONE', #6049, #14250, #20273 ) ;
#916=CARTESIAN_POINT ( 'NONE',  ( -52.23920841373872292, 126.9191314136037789, 167.5279203743774303 ) ) ;
#922=VERTEX_POINT ( 'NONE', #5610 ) ;
#1024=DIRECTION ( 'NONE',  ( -7.125109674403276030E-05, 0.9999848031710252272, -0.005512562950848280685 ) ) ;
#1027=UNCERTAINTY_MEASURE_WITH_UNIT (LENGTH_MEASURE( 1.000000000000000082E-05 ), #12937, 'distance_accuracy_value', 'NONE');
#1123=DIRECTION ( 'NONE',  ( 0.9999164797902015955, 0.000000000000000000, -0.01292414190464144692 ) ) ;
#1179=FACE_BOUND ( 'NONE', #18318, .T. ) ;
#1220=ORIENTED_EDGE ( 'NONE', *, *, #9901, .T. ) ;
#1257=ORIENTED_EDGE ( 'NONE', *, *, #2125, .T. ) ;
#1302=VERTEX_POINT ( 'NONE', #9675 ) ;
#1342=DIRECTION ( 'NONE',  ( 7.125109674403277385E-05, -0.9999848031710253382, 0.005512562950848281552 ) ) ;
#1395=DIRECTION ( 'NONE',  ( 1.000000000000000000, 0.000000000000000000, 0.000000000000000000 ) ) ;
#1446=CARTESIAN_POINT ( 'NONE',  ( -53.78951186480472302, 118.2576901802692788, 47.58386677032791567 ) ) ;
#1492=FACE_OUTER_BOUND ( 'NONE', #20573, .T. ) ;
#1513=ORIENTED_EDGE ( 'NONE', *, *, #20558, .T. ) ;
#1595=CARTESIAN_POINT ( 'NONE',  ( -55.33837949231439524, 118.9192529882355984, 167.6120857178885899 ) ) ;
#1605=PLANE ( 'NONE',  #17716 ) ;
#1659=ADVANCED_FACE ( 'NONE', ( #8831 ), #3447, .F. ) ;
#1686=ORIENTED_EDGE ( 'NONE', *, *, #9145, .F. ) ;
#1690=VECTOR ( 'NONE', #4472, 1000.000000000000227 ) ;
#1720=VERTEX_POINT ( 'NONE', #9293 ) ;
#1769=DIRECTION ( 'NONE',  ( 7.125109674403276030E-05, -0.9999848031710252272, 0.005512562950848280685 ) ) ;
#1800=ORIENTED_EDGE ( 'NONE', *, *, #21148, .F. ) ;
#1843=CARTESIAN_POINT ( 'NONE',  ( -59.98899403950397158, 118.2576901802692504, 47.66399645013669328 ) ) ;
#1904=VERTEX_POINT ( 'NONE', #21306 ) ;
#1928=DIRECTION ( 'NONE',  ( 7.125109674403276030E-05, -0.9999848031710252272, 0.005512562950848280685 ) ) ;
#1929=FACE_BOUND ( 'NONE', #434, .T. ) ;
#1932=FACE_OUTER_BOUND ( 'NONE', #2191, .T. ) ;
#1939=ORIENTED_EDGE ( 'NONE', *, *, #11044, .T. ) ;
#2036=FILL_AREA_STYLE_COLOUR ( '', #13310 ) ;
#2081=PRODUCT_CONTEXT ( 'NONE', #15292, 'mechanical' ) ;
#2118=EDGE_LOOP ( 'NONE', ( #1686, #12689, #13822, #81 ) ) ;
#2125=EDGE_CURVE ( 'NONE', #14118, #1904, #9858, .T. ) ;
#2191=EDGE_LOOP ( 'NONE', ( #5795, #8720, #20797, #9896 ) ) ;
#2285=CARTESIAN_POINT ( 'NONE',  ( -53.79008187357867854, 126.2575686056374735, 47.53976626672113071 ) ) ;
#2302=DIRECTION ( 'NONE',  ( -0.9999164797902015955, -4.476705744456278510E-15, 0.01292414190463697134 ) ) ;
#2453=CYLINDRICAL_SURFACE ( 'NONE', #20102, 3.099999999999998757 ) ;
#2483=FACE_OUTER_BOUND ( 'NONE', #17267, .T. ) ;
#2492=CYLINDRICAL_SURFACE ( 'NONE', #61, 3.099999999999998757 ) ;
#2609=EDGE_CURVE ( 'NONE', #922, #8505, #16862, .T. ) ;
#2641=EDGE_CURVE ( 'NONE', #5358, #1302, #19530, .T. ) ;
#2748=CARTESIAN_POINT ( 'NONE',  ( -59.21355730958399732, 118.5884715842524173, 107.6580735039648431 ) ) ;
#2792=DIRECTION ( 'NONE',  ( -0.9999164797902017066, -2.457127383503899093E-15, 0.01292414190464056742 ) ) ;
#3052=DIRECTION ( 'NONE',  ( 7.125109674403276030E-05, -0.9999848031710252272, 0.005512562950848280685 ) ) ;
#3066=VECTOR ( 'NONE', #8424, 999.9999999999998863 ) ;
#3093=DIRECTION ( 'NONE',  ( 0.9999164797902015955, 2.457859219970326020E-15, -0.01292414190464043211 ) ) ;
#3099=VERTEX_POINT ( 'NONE', #5046 ) ;
#3102=CARTESIAN_POINT ( 'NONE',  ( 0.000000000000000000, 0.000000000000000000, 0.000000000000000000 ) ) ;
#3241=ORIENTED_EDGE ( 'NONE', *, *, #9392, .F. ) ;
#3321=EDGE_CURVE ( 'NONE', #858, #12094, #737, .T. ) ;
#3341=VECTOR ( 'NONE', #3945, 1000.000000000000227 ) ;
#3346=VECTOR ( 'NONE', #13495, 999.9999999999998863 ) ;
#3447=PLANE ( 'NONE',  #5038 ) ;
#3456=CIRCLE ( 'NONE', #5279, 3.099999999999998757 ) ;
#3515=CARTESIAN_POINT ( 'NONE',  ( -56.88982296092829927, 126.2575686056374735, 47.57983110662551951 ) ) ;
#3597=DIRECTION ( 'NONE',  ( -0.9999164797902015955, -4.476705744456268255E-15, 0.01292414190464141917 ) ) ;
#3618=EDGE_CURVE ( 'NONE', #10046, #16057, #11285, .T. ) ;
#3742=EDGE_LOOP ( 'NONE', ( #1800, #1220, #22064, #18020 ) ) ;
#3758=DIRECTION ( 'NONE',  ( -7.125109674403282806E-05, 0.9999848031710253382, -0.005512562950848280685 ) ) ;
#3776=ORIENTED_EDGE ( 'NONE', *, *, #14294, .F. ) ;
#3813=LINE ( 'NONE', #17857, #9697 ) ;
#3922=LINE ( 'NONE', #7604, #13 ) ;
#3945=DIRECTION ( 'NONE',  ( -0.9999164797902015955, -2.457859219970326020E-15, 0.01292414190464043211 ) ) ;
#3962=PRESENTATION_STYLE_ASSIGNMENT (( #9022 ) ) ;
#3964=FACE_OUTER_BOUND ( 'NONE', #19952, .T. ) ;
#4127=ORIENTED_EDGE ( 'NONE', *, *, #19905, .F. ) ;
#4154=EDGE_LOOP ( 'NONE', ( #7510, #12307 ) ) ;
#4178=ADVANCED_FACE ( 'NONE', ( #20356 ), #2453, .F. ) ;
#4397=LINE ( 'NONE', #21617, #22013 ) ;
#4406=CIRCLE ( 'NONE', #12852, 3.099999999999998757 ) ;
#4472=DIRECTION ( 'NONE',  ( -0.9999164797902015955, -2.457859219970326020E-15, 0.01292414190464043211 ) ) ;
#4474=CARTESIAN_POINT ( 'NONE',  ( -59.98899403950397158, 118.2576901802692504, 47.66399645013669328 ) ) ;
#4501=DIRECTION ( 'NONE',  ( 7.125109674403277385E-05, -0.9999848031710253382, 0.005512562950848281552 ) ) ;
#4536=LINE ( 'NONE', #20611, #17608 ) ;
#4549=ORIENTED_EDGE ( 'NONE', *, *, #12097, .F. ) ;
#4571=CARTESIAN_POINT ( 'NONE',  ( -56.88982296092829927, 126.2575686056374735, 47.57983110662551951 ) ) ;
#4795=ORIENTED_EDGE ( 'NONE', *, *, #12097, .T. ) ;
#4812=CARTESIAN_POINT ( 'NONE',  ( -52.61410854296865836, 118.5884715842524457, 107.5727741673942148 ) ) ;
#4843=LINE ( 'NONE', #17061, #3346 ) ;
#5038=AXIS2_PLACEMENT_3D ( 'NONE', #7120, #15646, #12651 ) ;
#5046=CARTESIAN_POINT ( 'NONE',  ( -53.01464514365870428, 126.5883500096206262, 107.5338433205492805 ) ) ;
#5198=ORIENTED_EDGE ( 'NONE', *, *, #13085, .F. ) ;
#5201=MECHANICAL_DESIGN_GEOMETRIC_PRESENTATION_REPRESENTATION('',(#5933),#6321);
#5215=CARTESIAN_POINT ( 'NONE',  ( -64.64767546932813502, 126.1473081376430798, 27.67873648630093797 ) ) ;
#5230=LINE ( 'NONE', #4474, #8939 ) ;
#5279=AXIS2_PLACEMENT_3D ( 'NONE', #310, #12829, #14465 ) ;
#5280=AXIS2_PLACEMENT_3D ( 'NONE', #1595, #8463, #12046 ) ;
#5358=VERTEX_POINT ( 'NONE', #12675 ) ;
#5517=VERTEX_POINT ( 'NONE', #9043 ) ;
#5525=ORIENTED_EDGE ( 'NONE', *, *, #19905, .T. ) ;
#5585=SURFACE_STYLE_FILL_AREA ( #21094 ) ;
#5588=EDGE_LOOP ( 'NONE', ( #5762, #16200 ) ) ;
#5610=CARTESIAN_POINT ( 'NONE',  ( -52.23863840496477451, 118.9192529882356126, 167.5720208779842153 ) ) ;
#5621=CARTESIAN_POINT ( 'NONE',  ( -64.64710546055418661, 118.1474297122748709, 27.72283698990772649 ) ) ;
#5655=VERTEX_POINT ( 'NONE', #916 ) ;
#5657=AXIS2_PLACEMENT_3D ( 'NONE', #10429, #1928, #7085 ) ;
#5681=AXIS2_PLACEMENT_3D ( 'NONE', #13803, #8490, #17481 ) ;
#5750=CARTESIAN_POINT ( 'NONE',  ( -55.33837949231439524, 118.9192529882355984, 167.6120857178885899 ) ) ;
#5751=DIRECTION ( 'NONE',  ( 7.125109674403277385E-05, -0.9999848031710253382, 0.005512562950848281552 ) ) ;
#5762=ORIENTED_EDGE ( 'NONE', *, *, #8689, .F. ) ;
#5795=ORIENTED_EDGE ( 'NONE', *, *, #13085, .T. ) ;
#5803=FACE_BOUND ( 'NONE', #5588, .T. ) ;
#5809=AXIS2_PLACEMENT_3D ( 'NONE', #17411, #1769, #3597 ) ;
#5820=VECTOR ( 'NONE', #7344, 1000.000000000000114 ) ;
#5875=CARTESIAN_POINT ( 'NONE',  ( -64.64710546055418661, 118.1474297122748709, 27.72283698990772649 ) ) ;
#5933=STYLED_ITEM ( 'NONE', ( #3962 ), #17112 ) ;
#5993=EDGE_CURVE ( 'NONE', #1904, #14118, #13607, .T. ) ;
#6022=PLANE ( 'NONE',  #18368 ) ;
#6031=ORIENTED_EDGE ( 'NONE', *, *, #12663, .T. ) ;
#6049=CARTESIAN_POINT ( 'NONE',  ( -56.88925295215435085, 118.2576901802692646, 47.62393161023230448 ) ) ;
#6134=SHAPE_REPRESENTATION_RELATIONSHIP ( 'NONE' , 'NONE' ,  #17373, #14307 ) ;
#6292=AXIS2_PLACEMENT_3D ( 'NONE', #3102, #12069, #1395 ) ;
#6310=ADVANCED_FACE ( 'NONE', ( #14548 ), #6022, .F. ) ;
#6317=AXIS2_PLACEMENT_3D ( 'NONE', #4812, #22161, #7004 ) ;
#6321=( GEOMETRIC_REPRESENTATION_CONTEXT ( 3 ) GLOBAL_UNCERTAINTY_ASSIGNED_CONTEXT ( ( #14301 ) ) GLOBAL_UNIT_ASSIGNED_CONTEXT ( ( #12616, #7199, #13988 ) ) REPRESENTATION_CONTEXT ( 'NONE', 'WORKASPACE' ) );
#6325=VERTEX_POINT ( 'NONE', #18310 ) ;
#6345=ORIENTED_EDGE ( 'NONE', *, *, #8487, .F. ) ;
#6426=DIRECTION ( 'NONE',  ( -0.9999164797902015955, -4.476705744456278510E-15, 0.01292414190463697134 ) ) ;
#6669=EDGE_CURVE ( 'NONE', #8505, #922, #19820, .T. ) ;
#6710=CARTESIAN_POINT ( 'NONE',  ( -58.43869058843797148, 126.9191314136037789, 167.6080500541861795 ) ) ;
#6762=VECTOR ( 'NONE', #17567, 999.9999999999998863 ) ;
#6859=LINE ( 'NONE', #13884, #6762 ) ;
#6871=DIRECTION ( 'NONE',  ( -7.125109674403276030E-05, 0.9999848031710252272, -0.005512562950848280685 ) ) ;
#6941=AXIS2_PLACEMENT_3D ( 'NONE', #4571, #1024, #15397 ) ;
#7004=DIRECTION ( 'NONE',  ( 0.9999164797902015955, 2.457859219970326020E-15, -0.01292414190464043211 ) ) ;
#7030=ADVANCED_FACE ( 'NONE', ( #7989 ), #2492, .F. ) ;
#7085=DIRECTION ( 'NONE',  ( -0.9999164797902015955, -4.476705744456278510E-15, 0.01292414190464144692 ) ) ;
#7120=CARTESIAN_POINT ( 'NONE',  ( -64.64767546932813502, 126.1473081376430798, 27.67873648630093797 ) ) ;
#7199=( NAMED_UNIT ( * ) PLANE_ANGLE_UNIT ( ) SI_UNIT ( $, .RADIAN. ) );
#7201=CARTESIAN_POINT ( 'NONE',  ( -52.61467855174260677, 126.5883500096206546, 107.5286736637874299 ) ) ;
#7344=DIRECTION ( 'NONE',  ( -0.01292394549866637994, -0.005513023399719273882, -0.9999012842304692006 ) ) ;
#7419=DIRECTION ( 'NONE',  ( 0.9999164797902015955, 0.000000000000000000, -0.01292414190464144692 ) ) ;
#7494=CARTESIAN_POINT ( 'NONE',  ( -40.58168163415708563, 127.0293918815982011, 187.3786108412739395 ) ) ;
#7510=ORIENTED_EDGE ( 'NONE', *, *, #6669, .F. ) ;
#7522=( NAMED_UNIT ( * ) SI_UNIT ( $, .STERADIAN. ) SOLID_ANGLE_UNIT ( ) );
#7604=CARTESIAN_POINT ( 'NONE',  ( -64.64767546932813502, 126.1473081376430798, 27.67873648630093797 ) ) ;
#7614=CARTESIAN_POINT ( 'NONE',  ( -56.11381622223437660, 118.5884715842524315, 107.6180086640604543 ) ) ;
#7666=AXIS2_PLACEMENT_3D ( 'NONE', #21679, #16448, #2302 ) ;
#7808=VECTOR ( 'NONE', #5751, 999.9999999999998863 ) ;
#7852=EDGE_CURVE ( 'NONE', #3099, #6325, #19884, .T. ) ;
#7900=PRODUCT_DEFINITION ( 'UNKNOWN', '', #11387, #20744 ) ;
#7989=FACE_OUTER_BOUND ( 'NONE', #3742, .T. ) ;
#8127=VECTOR ( 'NONE', #9812, 1000.000000000000227 ) ;
#8424=DIRECTION ( 'NONE',  ( 7.125109674403277385E-05, -0.9999848031710253382, 0.005512562950848281552 ) ) ;
#8447=DIRECTION ( 'NONE',  ( 7.125109674403277385E-05, -0.9999848031710253382, 0.005512562950848281552 ) ) ;
#8463=DIRECTION ( 'NONE',  ( 7.125109674403277385E-05, -0.9999848031710253382, 0.005512562950848281552 ) ) ;
#8487=EDGE_CURVE ( 'NONE', #12028, #10294, #4406, .T. ) ;
#8490=DIRECTION ( 'NONE',  ( -7.125109674403276030E-05, 0.9999848031710252272, -0.005512562950848280685 ) ) ;
#8505=VERTEX_POINT ( 'NONE', #14236 ) ;
#8506=APPLICATION_CONTEXT ( 'automotive_design' ) ;
#8516=ADVANCED_FACE ( 'NONE', ( #1932 ), #14122, .F. ) ;
#8566=CARTESIAN_POINT ( 'NONE',  ( -56.11381622223437660, 118.5884715842524315, 107.6180086640604543 ) ) ;
#8579=AXIS2_PLACEMENT_3D ( 'NONE', #21825, #2792, #14981 ) ;
#8689=EDGE_CURVE ( 'NONE', #6325, #3099, #10292, .T. ) ;
#8720=ORIENTED_EDGE ( 'NONE', *, *, #13315, .T. ) ;
#8729=EDGE_LOOP ( 'NONE', ( #19939, #18243, #18960, #14611 ) ) ;
#8793=LINE ( 'NONE', #18017, #16208 ) ;
#8831=FACE_OUTER_BOUND ( 'NONE', #15637, .T. ) ;
#8844=PRODUCT ( 'Holder', 'Holder', '', ( #2081 ) ) ;
#8916=FACE_BOUND ( 'NONE', #16415, .T. ) ;
#8939=VECTOR ( 'NONE', #20208, 999.9999999999998863 ) ;
#9007=CARTESIAN_POINT ( 'NONE',  ( -42.64951291394369548, 126.1473081376431367, 27.39440536439884255 ) ) ;
#9022=SURFACE_STYLE_USAGE ( .BOTH. , #19695 ) ;
#9043=CARTESIAN_POINT ( 'NONE',  ( -42.64951291394369548, 126.1473081376431367, 27.39440536439884255 ) ) ;
#9145=EDGE_CURVE ( 'NONE', #3099, #10294, #4397, .T. ) ;
#9208=DIRECTION ( 'NONE',  ( 0.01292394549866637994, 0.005513023399719273882, 0.9999012842304692006 ) ) ;
#9293=CARTESIAN_POINT ( 'NONE',  ( -62.57984418954151806, 127.0293918815981442, 187.6629419631760243 ) ) ;
#9330=DIRECTION ( 'NONE',  ( 7.125109674403277385E-05, -0.9999848031710253382, 0.005512562950848281552 ) ) ;
#9352=ADVANCED_FACE ( 'NONE', ( #1929, #5803, #8916, #3964 ), #205, .T. ) ;
#9392=EDGE_CURVE ( 'NONE', #1720, #16057, #8793, .T. ) ;
#9397=EDGE_LOOP ( 'NONE', ( #6345, #4549 ) ) ;
#9444=EDGE_LOOP ( 'NONE', ( #10306, #20992, #4795, #19291 ) ) ;
#9666=CARTESIAN_POINT ( 'NONE',  ( -42.64894290516974706, 118.1474297122749135, 27.43850586800562752 ) ) ;
#9675=CARTESIAN_POINT ( 'NONE',  ( -42.64894290516974706, 118.1474297122749135, 27.43850586800562752 ) ) ;
#9697=VECTOR ( 'NONE', #21254, 999.9999999999998863 ) ;
#9812=DIRECTION ( 'NONE',  ( 0.9999164797902015955, 2.457859219970326020E-15, -0.01292414190464043211 ) ) ;
#9858=CIRCLE ( 'NONE', #5809, 3.100000000000005418 ) ;
#9889=FACE_BOUND ( 'NONE', #4154, .T. ) ;
#9896=ORIENTED_EDGE ( 'NONE', *, *, #20483, .F. ) ;
#9901=EDGE_CURVE ( 'NONE', #5655, #14473, #10103, .T. ) ;
#9938=AXIS2_PLACEMENT_3D ( 'NONE', #5750, #9980, #6426 ) ;
#9959=ORIENTED_EDGE ( 'NONE', *, *, #9392, .T. ) ;
#9980=DIRECTION ( 'NONE',  ( 7.125109674403276030E-05, -0.9999848031710252272, 0.005512562950848280685 ) ) ;
#10046=VERTEX_POINT ( 'NONE', #5621 ) ;
#10103=CIRCLE ( 'NONE', #5681, 3.099999999999998757 ) ;
#10255=LINE ( 'NONE', #13930, #17697 ) ;
#10292=CIRCLE ( 'NONE', #17286, 3.099999999999998757 ) ;
#10294=VERTEX_POINT ( 'NONE', #16014 ) ;
#10305=AXIS2_PLACEMENT_3D ( 'NONE', #7201, #3758, #10771 ) ;
#10306=ORIENTED_EDGE ( 'NONE', *, *, #8689, .T. ) ;
#10400=CARTESIAN_POINT ( 'NONE',  ( -40.58168163415708563, 127.0293918815982011, 187.3786108412739395 ) ) ;
#10429=CARTESIAN_POINT ( 'NONE',  ( -56.11381622223437660, 118.5884715842524315, 107.6180086640604543 ) ) ;
#10480=EDGE_CURVE ( 'NONE', #1302, #10046, #22148, .T. ) ;
#10514=LINE ( 'NONE', #10400, #21395 ) ;
#10694=( GEOMETRIC_REPRESENTATION_CONTEXT ( 3 ) GLOBAL_UNCERTAINTY_ASSIGNED_CONTEXT ( ( #1027 ) ) GLOBAL_UNIT_ASSIGNED_CONTEXT ( ( #12937, #11310, #7522 ) ) REPRESENTATION_CONTEXT ( 'NONE', 'WORKASPACE' ) );
#10771=DIRECTION ( 'NONE',  ( 0.9999164797902015955, 2.457859219970326020E-15, -0.01292414190464043211 ) ) ;
#10776=DIRECTION ( 'NONE',  ( -0.9999164797902015955, -4.476705744456278510E-15, 0.01292414190464144692 ) ) ;
#10780=ADVANCED_FACE ( 'NONE', ( #2483 ), #12643, .F. ) ;
#11044=EDGE_CURVE ( 'NONE', #1720, #20978, #10514, .T. ) ;
#11109=AXIS2_PLACEMENT_3D ( 'NONE', #8566, #8447, #15497 ) ;
#11176=EDGE_LOOP ( 'NONE', ( #1513, #38, #14935, #3776 ) ) ;
#11195=CARTESIAN_POINT ( 'NONE',  ( -64.64767546932813502, 126.1473081376430798, 27.67873648630093797 ) ) ;
#11285=LINE ( 'NONE', #5875, #297 ) ;
#11308=DIRECTION ( 'NONE',  ( -0.9999164797902015955, -2.457859219970326020E-15, 0.01292414190464043211 ) ) ;
#11310=( NAMED_UNIT ( * ) PLANE_ANGLE_UNIT ( ) SI_UNIT ( $, .RADIAN. ) );
#11348=EDGE_CURVE ( 'NONE', #6325, #12028, #3813, .T. ) ;
#11387=PRODUCT_DEFINITION_FORMATION_WITH_SPECIFIED_SOURCE ( 'ANY', '', #8844, .NOT_KNOWN. ) ;
#11393=AXIS2_PLACEMENT_3D ( 'NONE', #21099, #19601, #21211 ) ;
#11421=CARTESIAN_POINT ( 'NONE',  ( -40.58168163415708563, 127.0293918815982011, 187.3786108412739395 ) ) ;
#11559=LINE ( 'NONE', #1446, #3066 ) ;
#11675=CARTESIAN_POINT ( 'NONE',  ( -56.88925295215435085, 118.2576901802692646, 47.62393161023230448 ) ) ;
#11853=PLANE ( 'NONE',  #6317 ) ;
#12027=CYLINDRICAL_SURFACE ( 'NONE', #11109, 3.099999999999998757 ) ;
#12028=VERTEX_POINT ( 'NONE', #2748 ) ;
#12046=DIRECTION ( 'NONE',  ( -0.9999164797902015955, -4.476705744456278510E-15, 0.01292414190463697134 ) ) ;
#12060=CARTESIAN_POINT ( 'NONE',  ( -56.11438623100832501, 126.5883500096206262, 107.5739081604536693 ) ) ;
#12069=DIRECTION ( 'NONE',  ( 0.000000000000000000, 0.000000000000000000, 1.000000000000000000 ) ) ;
#12094=VERTEX_POINT ( 'NONE', #15171 ) ;
#12097=EDGE_CURVE ( 'NONE', #10294, #12028, #21430, .T. ) ;
#12143=FACE_OUTER_BOUND ( 'NONE', #2118, .T. ) ;
#12307=ORIENTED_EDGE ( 'NONE', *, *, #2609, .F. ) ;
#12327=ORIENTED_EDGE ( 'NONE', *, *, #2641, .T. ) ;
#12452=ORIENTED_EDGE ( 'NONE', *, *, #16832, .T. ) ;
#12616=( LENGTH_UNIT ( ) NAMED_UNIT ( * ) SI_UNIT ( .MILLI., .METRE. ) );
#12643=CYLINDRICAL_SURFACE ( 'NONE', #882, 3.099999999999998757 ) ;
#12651=DIRECTION ( 'NONE',  ( -0.01292394549866637994, -0.005513023399719273882, -0.9999012842304692006 ) ) ;
#12663=EDGE_CURVE ( 'NONE', #20978, #5358, #492, .T. ) ;
#12675=CARTESIAN_POINT ( 'NONE',  ( -40.58111162538312300, 119.0295134562300063, 187.4227113448806961 ) ) ;
#12689=ORIENTED_EDGE ( 'NONE', *, *, #7852, .T. ) ;
#12733=CARTESIAN_POINT ( 'NONE',  ( -56.11381622223437660, 118.5884715842524315, 107.6180086640604543 ) ) ;
#12829=DIRECTION ( 'NONE',  ( -7.125109674403276030E-05, 0.9999848031710252272, -0.005512562950848280685 ) ) ;
#12852=AXIS2_PLACEMENT_3D ( 'NONE', #12733, #21324, #10776 ) ;
#12937=( LENGTH_UNIT ( ) NAMED_UNIT ( * ) SI_UNIT ( .MILLI., .METRE. ) );
#12957=ORIENTED_EDGE ( 'NONE', *, *, #20558, .F. ) ;
#12995=VECTOR ( 'NONE', #625, 1000.000000000000114 ) ;
#13085=EDGE_CURVE ( 'NONE', #12094, #858, #17758, .T. ) ;
#13097=ORIENTED_EDGE ( 'NONE', *, *, #5993, .F. ) ;
#13155=LINE ( 'NONE', #18432, #8127 ) ;
#13252=ORIENTED_EDGE ( 'NONE', *, *, #3321, .T. ) ;
#13280=ORIENTED_EDGE ( 'NONE', *, *, #17423, .T. ) ;
#13310=COLOUR_RGB ( '', 0.09019608, 0.27058824, 0.51372549) ;
#13315=EDGE_CURVE ( 'NONE', #858, #1904, #11559, .T. ) ;
#13464=ORIENTED_EDGE ( 'NONE', *, *, #9901, .F. ) ;
#13495=DIRECTION ( 'NONE',  ( 7.125109674403277385E-05, -0.9999848031710253382, 0.005512562950848281552 ) ) ;
#13607=CIRCLE ( 'NONE', #14720, 3.100000000000005418 ) ;
#13803=CARTESIAN_POINT ( 'NONE',  ( -55.33894950108835076, 126.9191314136037789, 167.5679852142818334 ) ) ;
#13822=ORIENTED_EDGE ( 'NONE', *, *, #11348, .T. ) ;
#13858=ORIENTED_EDGE ( 'NONE', *, *, #3321, .F. ) ;
#13884=CARTESIAN_POINT ( 'NONE',  ( -58.43812057966402307, 118.9192529882355842, 167.6521505577929645 ) ) ;
#13930=CARTESIAN_POINT ( 'NONE',  ( -42.64951291394369548, 126.1473081376431367, 27.39440536439884255 ) ) ;
#13988=( NAMED_UNIT ( * ) SI_UNIT ( $, .STERADIAN. ) SOLID_ANGLE_UNIT ( ) );
#14031=ADVANCED_FACE ( 'NONE', ( #14883 ), #16927, .F. ) ;
#14118=VERTEX_POINT ( 'NONE', #1843 ) ;
#14122=CYLINDRICAL_SURFACE ( 'NONE', #11393, 3.099999999999998757 ) ;
#14236=CARTESIAN_POINT ( 'NONE',  ( -58.43812057966402307, 118.9192529882355842, 167.6521505577929645 ) ) ;
#14250=DIRECTION ( 'NONE',  ( 7.125109674403277385E-05, -0.9999848031710253382, 0.005512562950848281552 ) ) ;
#14271=ADVANCED_FACE ( 'NONE', ( #19380 ), #17338, .F. ) ;
#14294=EDGE_CURVE ( 'NONE', #14473, #8505, #6859, .T. ) ;
#14301=UNCERTAINTY_MEASURE_WITH_UNIT (LENGTH_MEASURE( 1.000000000000000082E-05 ), #12616, 'distance_accuracy_value', 'NONE');
#14307=ADVANCED_BREP_SHAPE_REPRESENTATION ( '', ( #17112, #6292 ), #10694 ) ;
#14362=ORIENTED_EDGE ( 'NONE', *, *, #15691, .T. ) ;
#14465=DIRECTION ( 'NONE',  ( 0.9999164797902015955, 0.000000000000000000, -0.01292414190463697134 ) ) ;
#14473=VERTEX_POINT ( 'NONE', #6710 ) ;
#14548=FACE_OUTER_BOUND ( 'NONE', #16169, .T. ) ;
#14611=ORIENTED_EDGE ( 'NONE', *, *, #2641, .F. ) ;
#14720=AXIS2_PLACEMENT_3D ( 'NONE', #11675, #3052, #16978 ) ;
#14883=FACE_OUTER_BOUND ( 'NONE', #15463, .T. ) ;
#14935=ORIENTED_EDGE ( 'NONE', *, *, #2609, .T. ) ;
#14981=DIRECTION ( 'NONE',  ( 0.01292394549866637994, 0.005513023399719273882, 0.9999012842304692006 ) ) ;
#15030=DIRECTION ( 'NONE',  ( -0.9999164797902015955, -4.476705744456278510E-15, 0.01292414190463697134 ) ) ;
#15171=CARTESIAN_POINT ( 'NONE',  ( -59.98956404827792710, 126.2575686056374735, 47.61989594652990831 ) ) ;
#15292=APPLICATION_CONTEXT ( 'automotive_design' ) ;
#15397=DIRECTION ( 'NONE',  ( 0.9999164797902015955, 0.000000000000000000, -0.01292414190464144692 ) ) ;
#15463=EDGE_LOOP ( 'NONE', ( #12327, #1, #19432, #6031 ) ) ;
#15497=DIRECTION ( 'NONE',  ( -0.9999164797902015955, -4.476705744456278510E-15, 0.01292414190464144692 ) ) ;
#15504=ORIENTED_EDGE ( 'NONE', *, *, #13315, .F. ) ;
#15637=EDGE_LOOP ( 'NONE', ( #18130, #3241, #4127, #14362 ) ) ;
#15646=DIRECTION ( 'NONE',  ( 0.9999164797902017066, 2.457127383503899093E-15, -0.01292414190464056742 ) ) ;
#15691=EDGE_CURVE ( 'NONE', #16093, #10046, #3922, .T. ) ;
#15846=DIRECTION ( 'NONE',  ( 7.125109674403277385E-05, -0.9999848031710253382, 0.005512562950848281552 ) ) ;
#15954=DIRECTION ( 'NONE',  ( -7.125109674403276030E-05, 0.9999848031710252272, -0.005512562950848280685 ) ) ;
#16005=EDGE_CURVE ( 'NONE', #5517, #16093, #16289, .T. ) ;
#16014=CARTESIAN_POINT ( 'NONE',  ( -53.01407513488474876, 118.5884715842524457, 107.5779438241560655 ) ) ;
#16057=VERTEX_POINT ( 'NONE', #19676 ) ;
#16093=VERTEX_POINT ( 'NONE', #5215 ) ;
#16169=EDGE_LOOP ( 'NONE', ( #16584, #17847, #834, #9959 ) ) ;
#16200=ORIENTED_EDGE ( 'NONE', *, *, #7852, .F. ) ;
#16208=VECTOR ( 'NONE', #15846, 999.9999999999998863 ) ;
#16277=CLOSED_SHELL ( 'NONE', ( #8516, #4178, #14271, #18061, #6310, #14031, #18826, #1659, #9352, #7030, #19309, #10780 ) ) ;
#16289=LINE ( 'NONE', #9007, #3341 ) ;
#16415=EDGE_LOOP ( 'NONE', ( #12957, #13464 ) ) ;
#16448=DIRECTION ( 'NONE',  ( 7.125109674403276030E-05, -0.9999848031710252272, 0.005512562950848280685 ) ) ;
#16584=ORIENTED_EDGE ( 'NONE', *, *, #21082, .T. ) ;
#16654=ORIENTED_EDGE ( 'NONE', *, *, #15691, .F. ) ;
#16832=EDGE_CURVE ( 'NONE', #20978, #5517, #10255, .T. ) ;
#16862=CIRCLE ( 'NONE', #7666, 3.099999999999998757 ) ;
#16913=FACE_BOUND ( 'NONE', #9397, .T. ) ;
#16927=PLANE ( 'NONE',  #8579 ) ;
#16978=DIRECTION ( 'NONE',  ( -0.9999164797902015955, -4.476705744456268255E-15, 0.01292414190464141917 ) ) ;
#17023=DIRECTION ( 'NONE',  ( 0.9999164797902015955, 0.000000000000000000, -0.01292414190464144692 ) ) ;
#17061=CARTESIAN_POINT ( 'NONE',  ( -52.23863840496477451, 118.9192529882356126, 167.5720208779842153 ) ) ;
#17112=MANIFOLD_SOLID_BREP ( 'Stock-MAS-425-1', #16277 ) ;
#17267=EDGE_LOOP ( 'NONE', ( #15504, #13252, #19612, #1257 ) ) ;
#17286=AXIS2_PLACEMENT_3D ( 'NONE', #18465, #20159, #1123 ) ;
#17338=CYLINDRICAL_SURFACE ( 'NONE', #5280, 3.099999999999998757 ) ;
#17373=SHAPE_REPRESENTATION ( 'Holder', ( #6292 ), #10694 ) ;
#17411=CARTESIAN_POINT ( 'NONE',  ( -56.88925295215435085, 118.2576901802692646, 47.62393161023230448 ) ) ;
#17423=EDGE_CURVE ( 'NONE', #5517, #1302, #4536, .T. ) ;
#17473=ORIENTED_EDGE ( 'NONE', *, *, #2125, .F. ) ;
#17481=DIRECTION ( 'NONE',  ( 0.9999164797902015955, 0.000000000000000000, -0.01292414190463697134 ) ) ;
#17567=DIRECTION ( 'NONE',  ( 7.125109674403277385E-05, -0.9999848031710253382, 0.005512562950848281552 ) ) ;
#17608=VECTOR ( 'NONE', #1342, 999.9999999999998863 ) ;
#17697=VECTOR ( 'NONE', #20924, 1000.000000000000114 ) ;
#17716=AXIS2_PLACEMENT_3D ( 'NONE', #22469, #22354, #3093 ) ;
#17758=CIRCLE ( 'NONE', #19907, 3.099999999999998757 ) ;
#17847=ORIENTED_EDGE ( 'NONE', *, *, #12663, .F. ) ;
#17857=CARTESIAN_POINT ( 'NONE',  ( -59.21355730958399732, 118.5884715842524173, 107.6580735039648431 ) ) ;
#18017=CARTESIAN_POINT ( 'NONE',  ( -62.57984418954151806, 127.0293918815981442, 187.6629419631760243 ) ) ;
#18020=ORIENTED_EDGE ( 'NONE', *, *, #6669, .T. ) ;
#18061=ADVANCED_FACE ( 'NONE', ( #20550, #9889, #16913, #1179 ), #11853, .F. ) ;
#18130=ORIENTED_EDGE ( 'NONE', *, *, #3618, .T. ) ;
#18243=ORIENTED_EDGE ( 'NONE', *, *, #3618, .F. ) ;
#18310=CARTESIAN_POINT ( 'NONE',  ( -59.21412731835795284, 126.5883500096206262, 107.6139730003580581 ) ) ;
#18318=EDGE_LOOP ( 'NONE', ( #17473, #13097 ) ) ;
#18338=CARTESIAN_POINT ( 'NONE',  ( -55.33837949231439524, 118.9192529882355984, 167.6120857178885899 ) ) ;
#18368=AXIS2_PLACEMENT_3D ( 'NONE', #11421, #630, #11308 ) ;
#18420=DIRECTION ( 'NONE',  ( -0.9999164797902015955, -4.476705744456278510E-15, 0.01292414190464144692 ) ) ;
#18432=CARTESIAN_POINT ( 'NONE',  ( -40.58111162538312300, 119.0295134562300063, 187.4227113448806961 ) ) ;
#18465=CARTESIAN_POINT ( 'NONE',  ( -56.11438623100832501, 126.5883500096206262, 107.5739081604536693 ) ) ;
#18801=AXIS2_PLACEMENT_3D ( 'NONE', #12060, #6871, #17023 ) ;
#18826=ADVANCED_FACE ( 'NONE', ( #1492 ), #1605, .F. ) ;
#18960=ORIENTED_EDGE ( 'NONE', *, *, #10480, .F. ) ;
#19158=ORIENTED_EDGE ( 'NONE', *, *, #16005, .F. ) ;
#19291=ORIENTED_EDGE ( 'NONE', *, *, #11348, .F. ) ;
#19309=ADVANCED_FACE ( 'NONE', ( #12143 ), #12027, .F. ) ;
#19380=FACE_OUTER_BOUND ( 'NONE', #11176, .T. ) ;
#19432=ORIENTED_EDGE ( 'NONE', *, *, #16832, .F. ) ;
#19512=ORIENTED_EDGE ( 'NONE', *, *, #10480, .T. ) ;
#19530=LINE ( 'NONE', #353, #5820 ) ;
#19601=DIRECTION ( 'NONE',  ( 7.125109674403277385E-05, -0.9999848031710253382, 0.005512562950848281552 ) ) ;
#19612=ORIENTED_EDGE ( 'NONE', *, *, #20483, .T. ) ;
#19676=CARTESIAN_POINT ( 'NONE',  ( -62.57927418076755544, 119.0295134562299637, 187.7070424667828377 ) ) ;
#19695=SURFACE_SIDE_STYLE ('',( #5585 ) ) ;
#19775=LINE ( 'NONE', #11195, #12995 ) ;
#19820=CIRCLE ( 'NONE', #9938, 3.099999999999998757 ) ;
#19884=CIRCLE ( 'NONE', #18801, 3.099999999999998757 ) ;
#19905=EDGE_CURVE ( 'NONE', #16093, #1720, #19775, .T. ) ;
#19907=AXIS2_PLACEMENT_3D ( 'NONE', #3515, #15954, #7419 ) ;
#19908=DIRECTION ( 'NONE',  ( 7.125109674403277385E-05, -0.9999848031710253382, 0.005512562950848281552 ) ) ;
#19939=ORIENTED_EDGE ( 'NONE', *, *, #21082, .F. ) ;
#19952=EDGE_LOOP ( 'NONE', ( #1939, #12452, #21486, #5525 ) ) ;
#20102=AXIS2_PLACEMENT_3D ( 'NONE', #7614, #4501, #18420 ) ;
#20159=DIRECTION ( 'NONE',  ( -7.125109674403276030E-05, 0.9999848031710252272, -0.005512562950848280685 ) ) ;
#20208=DIRECTION ( 'NONE',  ( 7.125109674403277385E-05, -0.9999848031710253382, 0.005512562950848281552 ) ) ;
#20273=DIRECTION ( 'NONE',  ( -0.9999164797902015955, -4.476705744456278510E-15, 0.01292414190464144692 ) ) ;
#20356=FACE_OUTER_BOUND ( 'NONE', #9444, .T. ) ;
#20483=EDGE_CURVE ( 'NONE', #12094, #14118, #5230, .T. ) ;
#20550=FACE_OUTER_BOUND ( 'NONE', #8729, .T. ) ;
#20558=EDGE_CURVE ( 'NONE', #14473, #5655, #3456, .T. ) ;
#20573=EDGE_LOOP ( 'NONE', ( #19512, #16654, #19158, #13280 ) ) ;
#20611=CARTESIAN_POINT ( 'NONE',  ( -42.64951291394369548, 126.1473081376431367, 27.39440536439884255 ) ) ;
#20744=PRODUCT_DEFINITION_CONTEXT ( 'detailed design', #8506, 'design' ) ;
#20797=ORIENTED_EDGE ( 'NONE', *, *, #5993, .T. ) ;
#20924=DIRECTION ( 'NONE',  ( -0.01292394549866637994, -0.005513023399719273882, -0.9999012842304692006 ) ) ;
#20978=VERTEX_POINT ( 'NONE', #22536 ) ;
#20992=ORIENTED_EDGE ( 'NONE', *, *, #9145, .T. ) ;
#21071=DIRECTION ( 'NONE',  ( 0.9999164797902015955, 2.457859219970326020E-15, -0.01292414190464043211 ) ) ;
#21082=EDGE_CURVE ( 'NONE', #16057, #5358, #13155, .T. ) ;
#21094=FILL_AREA_STYLE ('',( #2036 ) ) ;
#21099=CARTESIAN_POINT ( 'NONE',  ( -56.88925295215435085, 118.2576901802692646, 47.62393161023230448 ) ) ;
#21148=EDGE_CURVE ( 'NONE', #5655, #922, #4843, .T. ) ;
#21211=DIRECTION ( 'NONE',  ( -0.9999164797902015955, -4.476705744456278510E-15, 0.01292414190464144692 ) ) ;
#21254=DIRECTION ( 'NONE',  ( 7.125109674403277385E-05, -0.9999848031710253382, 0.005512562950848281552 ) ) ;
#21306=CARTESIAN_POINT ( 'NONE',  ( -53.78951186480472302, 118.2576901802692788, 47.58386677032791567 ) ) ;
#21324=DIRECTION ( 'NONE',  ( 7.125109674403276030E-05, -0.9999848031710252272, 0.005512562950848280685 ) ) ;
#21395=VECTOR ( 'NONE', #21071, 1000.000000000000227 ) ;
#21430=CIRCLE ( 'NONE', #5657, 3.099999999999998757 ) ;
#21486=ORIENTED_EDGE ( 'NONE', *, *, #16005, .T. ) ;
#21617=CARTESIAN_POINT ( 'NONE',  ( -53.01407513488474876, 118.5884715842524457, 107.5779438241560655 ) ) ;
#21644=DIRECTION ( 'NONE',  ( 7.125109674403277385E-05, -0.9999848031710253382, 0.005512562950848281552 ) ) ;
#21679=CARTESIAN_POINT ( 'NONE',  ( -55.33837949231439524, 118.9192529882355984, 167.6120857178885899 ) ) ;
#21825=CARTESIAN_POINT ( 'NONE',  ( -42.64951291394369548, 126.1473081376431367, 27.39440536439884255 ) ) ;
#21992=PRODUCT_DEFINITION_SHAPE ( 'NONE', 'NONE',  #7900 ) ;
#22013=VECTOR ( 'NONE', #19908, 999.9999999999998863 ) ;
#22064=ORIENTED_EDGE ( 'NONE', *, *, #14294, .T. ) ;
#22148=LINE ( 'NONE', #9666, #1690 ) ;
#22161=DIRECTION ( 'NONE',  ( -7.125109674403282806E-05, 0.9999848031710253382, -0.005512562950848280685 ) ) ;
#22246=SHAPE_DEFINITION_REPRESENTATION ( #21992, #17373 ) ;
#22354=DIRECTION ( 'NONE',  ( 0.01292394549866624984, 0.005513023399719273882, 0.9999012842304693116 ) ) ;
#22469=CARTESIAN_POINT ( 'NONE',  ( -42.64951291394369548, 126.1473081376431367, 27.39440536439884255 ) ) ;
#22536=CARTESIAN_POINT ( 'NONE',  ( -40.58168163415708563, 127.0293918815982011, 187.3786108412739395 ) ) ;
ENDSEC;
END-ISO-10303-21;
